ISO-10303-21;
HEADER;
/* Generated by software containing ST-Developer
 * from STEP Tools, Inc. (www.steptools.com) 
 */

FILE_DESCRIPTION(
/* description */ ('Belt tensioner idler arm'),
/* implementation_level */ '2;1');

FILE_NAME(
/* name */ 'M3 pulley set screw (1).step',
/* time_stamp */ '2026-10-28T03:22:15-07:00',
/* author */ (''),
/* organization */ (''),
/* preprocessor_version */ 'ST-DEVELOPER v20.2',
/* originating_system */ 'Autodesk Translation Framework v15.17.0.0',
/* authorisation */ '');

FILE_SCHEMA (('AUTOMOTIVE_DESIGN { 1 0 10303 214 3 1 1 }'));
ENDSEC;

DATA;
#10=MECHANICAL_DESIGN_GEOMETRIC_PRESENTATION_REPRESENTATION('',(#484),#12779);
#408=SHAPE_REPRESENTATION_RELATIONSHIP('SRR','None',#12957,#442);
#442=ADVANCED_BREP_SHAPE_REPRESENTATION('',(#523),#12774);
#484=STYLED_ITEM('',(#13191),#523);
#523=MANIFOLD_SOLID_BREP('Body1',#6221);
#808=PLANE('',#7209);
#809=PLANE('',#7210);
#1117=FACE_OUTER_BOUND('',#1605,.T.);
#1118=FACE_OUTER_BOUND('',#1606,.T.);
#1119=FACE_OUTER_BOUND('',#1607,.T.);
#1605=EDGE_LOOP('',(#5218,#5219,#5220,#5221));
#1606=EDGE_LOOP('',(#5222));
#1607=EDGE_LOOP('',(#5223));
#1960=LINE('',#11931,#2309);
#2309=VECTOR('',#8898,0.15);
#2665=CIRCLE('',#7207,0.15);
#2666=CIRCLE('',#7208,0.15);
#3148=VERTEX_POINT('',#11928);
#3149=VERTEX_POINT('',#11930);
#3864=EDGE_CURVE('',#3148,#3148,#2665,.T.);
#3865=EDGE_CURVE('',#3148,#3149,#1960,.T.);
#3866=EDGE_CURVE('',#3149,#3149,#2666,.T.);
#5218=ORIENTED_EDGE('',*,*,#3864,.F.);
#5219=ORIENTED_EDGE('',*,*,#3865,.T.);
#5220=ORIENTED_EDGE('',*,*,#3866,.T.);
#5221=ORIENTED_EDGE('',*,*,#3865,.F.);
#5222=ORIENTED_EDGE('',*,*,#3864,.T.);
#5223=ORIENTED_EDGE('',*,*,#3866,.F.);
#5760=CYLINDRICAL_SURFACE('',#7206,0.15);
#6094=ADVANCED_FACE('',(#1117),#5760,.T.);
#6095=ADVANCED_FACE('',(#1118),#808,.T.);
#6096=ADVANCED_FACE('',(#1119),#809,.F.);
#6221=CLOSED_SHELL('',(#6094,#6095,#6096));
#7205=AXIS2_PLACEMENT_3D('',#11926,#8892,#8893);
#7206=AXIS2_PLACEMENT_3D('',#11927,#8894,#8895);
#7207=AXIS2_PLACEMENT_3D('',#11929,#8896,#8897);
#7208=AXIS2_PLACEMENT_3D('',#11932,#8899,#8900);
#7209=AXIS2_PLACEMENT_3D('',#11933,#8901,#8902);
#7210=AXIS2_PLACEMENT_3D('',#11934,#8903,#8904);
#8892=DIRECTION('axis',(0.,0.,1.));
#8893=DIRECTION('refdir',(1.,0.,0.));
#8894=DIRECTION('center_axis',(1.,0.,0.));
#8895=DIRECTION('ref_axis',(0.,0.,-1.));
#8896=DIRECTION('center_axis',(1.,0.,0.));
#8897=DIRECTION('ref_axis',(0.,0.,-1.));
#8898=DIRECTION('',(-1.,0.,0.));
#8899=DIRECTION('center_axis',(1.,0.,0.));
#8900=DIRECTION('ref_axis',(0.,0.,-1.));
#8901=DIRECTION('center_axis',(1.,0.,0.));
#8902=DIRECTION('ref_axis',(0.,0.,-1.));
#8903=DIRECTION('center_axis',(1.,0.,0.));
#8904=DIRECTION('ref_axis',(0.,0.,-1.));
#11926=CARTESIAN_POINT('',(0.,0.,0.));
#11927=CARTESIAN_POINT('Origin',(9.4,0.,7.55));
#11928=CARTESIAN_POINT('',(9.65,-1.83697019872103E-17,7.7));
#11929=CARTESIAN_POINT('Origin',(9.65,0.,7.55));
#11930=CARTESIAN_POINT('',(9.4,-1.83697019872103E-17,7.7));
#11931=CARTESIAN_POINT('',(9.4,-1.83697019872103E-17,7.7));
#11932=CARTESIAN_POINT('Origin',(9.4,0.,7.55));
#11933=CARTESIAN_POINT('Origin',(9.65,0.,7.55));
#11934=CARTESIAN_POINT('Origin',(9.4,0.,7.55));
#12734=UNCERTAINTY_MEASURE_WITH_UNIT(LENGTH_MEASURE(0.001),#12780,
'DISTANCE_ACCURACY_VALUE',
'Maximum model space distance between geometric entities at asserted c
onnectivities');
#12739=UNCERTAINTY_MEASURE_WITH_UNIT(LENGTH_MEASURE(0.001),#12780,
'DISTANCE_ACCURACY_VALUE',
'Maximum model space distance between geometric entities at asserted c
onnectivities');
#12774=(
GEOMETRIC_REPRESENTATION_CONTEXT(3)
GLOBAL_UNCERTAINTY_ASSIGNED_CONTEXT((#12734))
GLOBAL_UNIT_ASSIGNED_CONTEXT((#12780,#12782,#12783))
REPRESENTATION_CONTEXT('','3D')
);
#12779=(
GEOMETRIC_REPRESENTATION_CONTEXT(3)
GLOBAL_UNCERTAINTY_ASSIGNED_CONTEXT((#12739))
GLOBAL_UNIT_ASSIGNED_CONTEXT((#12780,#12782,#12783))
REPRESENTATION_CONTEXT('','3D')
);
#12780=(
LENGTH_UNIT()
NAMED_UNIT(*)
SI_UNIT(.CENTI.,.METRE.)
);
#12782=(
NAMED_UNIT(*)
PLANE_ANGLE_UNIT()
SI_UNIT($,.RADIAN.)
);
#12783=(
NAMED_UNIT(*)
SI_UNIT($,.STERADIAN.)
SOLID_ANGLE_UNIT()
);
#12818=SHAPE_DEFINITION_REPRESENTATION(#12886,#12957);
#12886=PRODUCT_DEFINITION_SHAPE('',$,#12997);
#12957=SHAPE_REPRESENTATION('',(#7205),#12774);
#12962=PRODUCT_DEFINITION_CONTEXT('part definition',#13081,'design');
#12997=PRODUCT_DEFINITION('M3 pulley set screw (1)',
'M3 pulley set screw (1)',#13036,#12962);
#13036=PRODUCT_DEFINITION_FORMATION('',$,#13117);
#13081=APPLICATION_CONTEXT(
'Core Data for Automotive Mechanical Design Process');
#13082=PRODUCT_CONTEXT('part definition',#13081,'mechanical');
#13117=PRODUCT('M3 pulley set screw (1)','M3 pulley set screw (1)',
'M3 pulley set screw (1)',(#13082));
#13185=COLOUR_RGB('Black',0.12,0.14,0.17);
#13186=FILL_AREA_STYLE_COLOUR('',#13185);
#13187=FILL_AREA_STYLE('',(#13186));
#13188=SURFACE_STYLE_FILL_AREA(#13187);
#13189=SURFACE_SIDE_STYLE('',(#13188));
#13190=SURFACE_STYLE_USAGE(.BOTH.,#13189);
#13191=PRESENTATION_STYLE_ASSIGNMENT((#13190));
ENDSEC;
END-ISO-10303-21;
